ISO-10303-21;
HEADER;
FILE_DESCRIPTION (('STEP AP214'),
    '1' );
FILE_NAME ('Part9^Assem2.step',
    '2026-11-01T05:08:46',
    ( '' ),
    ( '' ),
    'SwSTEP 2.0',
    'SolidWorks 2024',
    '' );
FILE_SCHEMA (( 'AUTOMOTIVE_DESIGN' ));
ENDSEC;

DATA;
#1=EDGE_CURVE ( 'NONE', #6268, #16000, #1193, .T. ) ;
#90=EDGE_CURVE ( 'NONE', #3294, #11672, #5469, .T. ) ;
#99=CARTESIAN_POINT ( 'NONE',  ( 39.72345254347678889, 303.2115381654813859, -6.736600000000000144 ) ) ;
#103=AXIS2_PLACEMENT_3D ( 'NONE', #2236, #11104, #4571 ) ;
#113=( NAMED_UNIT ( * ) SI_UNIT ( $, .STERADIAN. ) SOLID_ANGLE_UNIT ( ) );
#192=ORIENTED_EDGE ( 'NONE', *, *, #5939, .F. ) ;
#195=SURFACE_SIDE_STYLE ('',( #12120 ) ) ;
#277=ORIENTED_EDGE ( 'NONE', *, *, #3429, .F. ) ;
#359=PRESENTATION_STYLE_ASSIGNMENT (( #5414 ) ) ;
#388=ADVANCED_FACE ( 'NONE', ( #12778 ), #10369, .T. ) ;
#396=DIRECTION ( 'NONE',  ( -0.9998870921963913805, -0.01502673813723916403, 0.000000000000000000 ) ) ;
#426=AXIS2_PLACEMENT_3D ( 'NONE', #9950, #15186, #14849 ) ;
#444=LINE ( 'NONE', #13585, #11069 ) ;
#448=AXIS2_PLACEMENT_3D ( 'NONE', #9388, #14975, #8100 ) ;
#450=( NAMED_UNIT ( * ) PLANE_ANGLE_UNIT ( ) SI_UNIT ( $, .RADIAN. ) );
#592=CARTESIAN_POINT ( 'NONE',  ( 415.0210210471910841, 329.6061121441327941, 0.000000000000000000 ) ) ;
#716=EDGE_CURVE ( 'NONE', #7408, #2249, #7077, .T. ) ;
#820=LINE ( 'NONE', #2010, #3272 ) ;
#999=CARTESIAN_POINT ( 'NONE',  ( 39.41161623800082481, 323.9612906317821057, 0.000000000000000000 ) ) ;
#1009=DIRECTION ( 'NONE',  ( 1.000000000000000000, 0.000000000000000000, 0.000000000000000000 ) ) ;
#1011=CARTESIAN_POINT ( 'NONE',  ( 39.75350601975127063, 301.2117639810886089, -6.736600000000000144 ) ) ;
#1017=CARTESIAN_POINT ( 'NONE',  ( 39.72345254347677468, 303.2115381654813859, 0.000000000000000000 ) ) ;
#1112=CARTESIAN_POINT ( 'NONE',  ( 435.7731165870194445, 329.6061121441327941, -6.736600000000000144 ) ) ;
#1120=CYLINDRICAL_SURFACE ( 'NONE', #3661, 20.75209553982835331 ) ;
#1132=VERTEX_POINT ( 'NONE', #1112 ) ;
#1190=AXIS2_PLACEMENT_3D ( 'NONE', #15516, #3825, #7593 ) ;
#1193=LINE ( 'NONE', #5134, #4445 ) ;
#1236=AXIS2_PLACEMENT_3D ( 'NONE', #592, #16216, #5908 ) ;
#1256=VECTOR ( 'NONE', #9148, 1000.000000000000000 ) ;
#1283=ORIENTED_EDGE ( 'NONE', *, *, #7902, .F. ) ;
#1308=CARTESIAN_POINT ( 'NONE',  ( 39.75350601975127063, 301.2117639810886089, 0.000000000000000000 ) ) ;
#1317=EDGE_CURVE ( 'NONE', #8414, #2249, #4170, .T. ) ;
#1321=ORIENTED_EDGE ( 'NONE', *, *, #14943, .T. ) ;
#1385=ORIENTED_EDGE ( 'NONE', *, *, #5385, .F. ) ;
#1387=( LENGTH_UNIT ( ) NAMED_UNIT ( * ) SI_UNIT ( .MILLI., .METRE. ) );
#1407=EDGE_LOOP ( 'NONE', ( #8814, #8708, #16892, #8161 ) ) ;
#1486=DIRECTION ( 'NONE',  ( 0.9998870921963913805, 0.01502673813723916230, 0.000000000000000000 ) ) ;
#1488=AXIS2_PLACEMENT_3D ( 'NONE', #3280, #8693, #15217 ) ;
#1528=DIRECTION ( 'NONE',  ( 0.000000000000000000, 0.000000000000000000, 1.000000000000000000 ) ) ;
#1617=CARTESIAN_POINT ( 'NONE',  ( 414.7091847417151484, 350.3558646104334571, -10.00000000000000000 ) ) ;
#1668=EDGE_LOOP ( 'NONE', ( #1824, #8368, #1872, #8991, #277 ) ) ;
#1706=ORIENTED_EDGE ( 'NONE', *, *, #1, .T. ) ;
#1730=ORIENTED_EDGE ( 'NONE', *, *, #9551, .F. ) ;
#1824=ORIENTED_EDGE ( 'NONE', *, *, #8247, .F. ) ;
#1850=CARTESIAN_POINT ( 'NONE',  ( 414.6791312654406738, 352.3556387948262341, -6.736600000000000144 ) ) ;
#1872=ORIENTED_EDGE ( 'NONE', *, *, #14130, .F. ) ;
#1887=CARTESIAN_POINT ( 'NONE',  ( 39.72345254347677468, 303.2115381654813859, 0.000000000000000000 ) ) ;
#1958=EDGE_CURVE ( 'NONE', #3705, #9126, #12039, .T. ) ;
#2010=CARTESIAN_POINT ( 'NONE',  ( 39.72345254347677468, 303.2115381654813859, -10.00000000000000000 ) ) ;
#2044=DIRECTION ( 'NONE',  ( -0.9998870921963913805, -0.01502673813723916056, 0.000000000000000000 ) ) ;
#2048=ORIENTED_EDGE ( 'NONE', *, *, #15763, .T. ) ;
#2059=EDGE_LOOP ( 'NONE', ( #15397, #6986, #8899, #7553, #1283 ) ) ;
#2107=VECTOR ( 'NONE', #12581, 1000.000000000000000 ) ;
#2112=UNCERTAINTY_MEASURE_WITH_UNIT (LENGTH_MEASURE( 1.000000000000000082E-05 ), #15978, 'distance_accuracy_value', 'NONE');
#2140=DIRECTION ( 'NONE',  ( 1.000000000000000000, 0.000000000000000000, 0.000000000000000000 ) ) ;
#2236=CARTESIAN_POINT ( 'NONE',  ( 415.0210210471910841, 329.6061121441327941, -6.736600000000000144 ) ) ;
#2249=VERTEX_POINT ( 'NONE', #5209 ) ;
#2324=ORIENTED_EDGE ( 'NONE', *, *, #6516, .T. ) ;
#2355=ORIENTED_EDGE ( 'NONE', *, *, #9623, .T. ) ;
#2361=CYLINDRICAL_SURFACE ( 'NONE', #1190, 22.75209553982836397 ) ;
#2366=VECTOR ( 'NONE', #7110, 1000.000000000000000 ) ;
#2385=EDGE_CURVE ( 'NONE', #3814, #4858, #820, .T. ) ;
#2403=FACE_OUTER_BOUND ( 'NONE', #9739, .T. ) ;
#2438=ORIENTED_EDGE ( 'NONE', *, *, #13739, .F. ) ;
#2486=AXIS2_PLACEMENT_3D ( 'NONE', #13123, #1528, #9259 ) ;
#2516=EDGE_CURVE ( 'NONE', #15471, #3705, #6279, .T. ) ;
#2727=DIRECTION ( 'NONE',  ( -0.9998870921963913805, -0.01502673813723915709, 0.000000000000000000 ) ) ;
#2781=ORIENTED_EDGE ( 'NONE', *, *, #2898, .T. ) ;
#2809=CARTESIAN_POINT ( 'NONE',  ( 414.6791312654406738, 352.3556387948262341, -6.736600000000000144 ) ) ;
#2816=EDGE_CURVE ( 'NONE', #4738, #8414, #7312, .T. ) ;
#2887=EDGE_CURVE ( 'NONE', #1132, #3294, #7480, .T. ) ;
#2898=EDGE_CURVE ( 'NONE', #4443, #7276, #7726, .T. ) ;
#2944=ORIENTED_EDGE ( 'NONE', *, *, #12222, .T. ) ;
#2993=DIRECTION ( 'NONE',  ( -0.000000000000000000, -0.000000000000000000, 1.000000000000000000 ) ) ;
#3045=VECTOR ( 'NONE', #14142, 1000.000000000000000 ) ;
#3046=ORIENTED_EDGE ( 'NONE', *, *, #5385, .T. ) ;
#3067=MANIFOLD_SOLID_BREP ( 'Cut-Extrude1', #3074 ) ;
#3074=CLOSED_SHELL ( 'NONE', ( #9568, #11936, #15248, #10089, #12949, #388, #9047, #7148, #3517, #15438, #16140, #12624 ) ) ;
#3272=VECTOR ( 'NONE', #3480, 1000.000000000000000 ) ;
#3280=CARTESIAN_POINT ( 'NONE',  ( 0.000000000000000000, 0.000000000000000000, 0.000000000000000000 ) ) ;
#3294=VERTEX_POINT ( 'NONE', #12099 ) ;
#3429=EDGE_CURVE ( 'NONE', #8130, #11672, #15421, .T. ) ;
#3464=ORIENTED_EDGE ( 'NONE', *, *, #9846, .F. ) ;
#3480=DIRECTION ( 'NONE',  ( -0.000000000000000000, -0.000000000000000000, 1.000000000000000000 ) ) ;
#3517=ADVANCED_FACE ( 'NONE', ( #11229 ), #16464, .F. ) ;
#3534=CYLINDRICAL_SURFACE ( 'NONE', #11002, 20.75209553982837463 ) ;
#3584=DIRECTION ( 'NONE',  ( 0.000000000000000000, 0.000000000000000000, 1.000000000000000000 ) ) ;
#3637=AXIS2_PLACEMENT_3D ( 'NONE', #999, #6291, #6215 ) ;
#3654=EDGE_LOOP ( 'NONE', ( #12440, #5094, #1321, #1730 ) ) ;
#3661=AXIS2_PLACEMENT_3D ( 'NONE', #6335, #10315, #15555 ) ;
#3665=FACE_OUTER_BOUND ( 'NONE', #1407, .T. ) ;
#3673=DIRECTION ( 'NONE',  ( 0.9998870921963913805, 0.01502673813723916403, 0.000000000000000000 ) ) ;
#3694=PRODUCT ( 'Part9^Assem2', 'Part9^Assem2', '', ( #10840 ) ) ;
#3705=VERTEX_POINT ( 'NONE', #10792 ) ;
#3814=VERTEX_POINT ( 'NONE', #14750 ) ;
#3825=DIRECTION ( 'NONE',  ( 0.000000000000000000, 0.000000000000000000, 1.000000000000000000 ) ) ;
#4022=DIRECTION ( 'NONE',  ( -0.000000000000000000, -0.000000000000000000, 1.000000000000000000 ) ) ;
#4086=FACE_OUTER_BOUND ( 'NONE', #9998, .T. ) ;
#4165=CARTESIAN_POINT ( 'NONE',  ( 39.72345254347677468, 303.2115381654813859, -10.00000000000000000 ) ) ;
#4170=CIRCLE ( 'NONE', #9939, 22.75209553982837463 ) ;
#4195=ORIENTED_EDGE ( 'NONE', *, *, #3429, .T. ) ;
#4204=EDGE_LOOP ( 'NONE', ( #10506, #5503, #4195, #7508 ) ) ;
#4237=EDGE_CURVE ( 'NONE', #4738, #7408, #9733, .T. ) ;
#4257=ORIENTED_EDGE ( 'NONE', *, *, #8247, .T. ) ;
#4375=CARTESIAN_POINT ( 'NONE',  ( 414.7091847417151484, 350.3558646104334571, -10.00000000000000000 ) ) ;
#4396=FILL_AREA_STYLE ('',( #8079 ) ) ;
#4403=ORIENTED_EDGE ( 'NONE', *, *, #12129, .F. ) ;
#4417=DIRECTION ( 'NONE',  ( 0.000000000000000000, 0.000000000000000000, 1.000000000000000000 ) ) ;
#4443=VERTEX_POINT ( 'NONE', #5217 ) ;
#4445=VECTOR ( 'NONE', #5211, 1000.000000000000000 ) ;
#4497=VECTOR ( 'NONE', #15229, 1000.000000000000000 ) ;
#4532=DIRECTION ( 'NONE',  ( 0.000000000000000000, 0.000000000000000000, 1.000000000000000000 ) ) ;
#4571=DIRECTION ( 'NONE',  ( 1.000000000000000000, 0.000000000000000000, 0.000000000000000000 ) ) ;
#4607=DIRECTION ( 'NONE',  ( 1.000000000000000000, 0.000000000000000000, 0.000000000000000000 ) ) ;
#4675=APPLICATION_CONTEXT ( 'automotive_design' ) ;
#4738=VERTEX_POINT ( 'NONE', #16219 ) ;
#4762=AXIS2_PLACEMENT_3D ( 'NONE', #16258, #11264, #5775 ) ;
#4820=CYLINDRICAL_SURFACE ( 'NONE', #103, 22.75209553982837463 ) ;
#4858=VERTEX_POINT ( 'NONE', #1017 ) ;
#4860=PRODUCT_DEFINITION_CONTEXT ( 'detailed design', #4675, 'design' ) ;
#4933=CARTESIAN_POINT ( 'NONE',  ( 415.0210210471910841, 329.6061121441327941, -6.736600000000000144 ) ) ;
#5049=CARTESIAN_POINT ( 'NONE',  ( 39.09977993252476836, 344.7110430980827687, 0.000000000000000000 ) ) ;
#5094=ORIENTED_EDGE ( 'NONE', *, *, #9882, .T. ) ;
#5134=CARTESIAN_POINT ( 'NONE',  ( 415.3328573526671335, 308.8563596778320743, -10.00000000000000000 ) ) ;
#5150=CARTESIAN_POINT ( 'NONE',  ( 39.09977993252476836, 344.7110430980827687, -10.00000000000000000 ) ) ;
#5154=ORIENTED_EDGE ( 'NONE', *, *, #1317, .F. ) ;
#5186=FACE_OUTER_BOUND ( 'NONE', #3654, .T. ) ;
#5209=CARTESIAN_POINT ( 'NONE',  ( 437.7731165870194445, 329.6061121441327941, 0.000000000000000000 ) ) ;
#5211=DIRECTION ( 'NONE',  ( -0.000000000000000000, -0.000000000000000000, 1.000000000000000000 ) ) ;
#5217=CARTESIAN_POINT ( 'NONE',  ( 39.09977993252476836, 344.7110430980827687, -6.736600000000000144 ) ) ;
#5248=DIRECTION ( 'NONE',  ( -0.9998870921963913805, -0.01502673813723916230, -0.000000000000000000 ) ) ;
#5274=DIRECTION ( 'NONE',  ( 0.01502673813723916403, -0.9998870921963913805, 0.000000000000000000 ) ) ;
#5385=EDGE_CURVE ( 'NONE', #5942, #10179, #9493, .T. ) ;
#5414=SURFACE_STYLE_USAGE ( .BOTH. , #195 ) ;
#5447=ORIENTED_EDGE ( 'NONE', *, *, #2385, .T. ) ;
#5466=ORIENTED_EDGE ( 'NONE', *, *, #12740, .T. ) ;
#5469=LINE ( 'NONE', #4375, #10193 ) ;
#5503=ORIENTED_EDGE ( 'NONE', *, *, #9846, .T. ) ;
#5555=APPLICATION_CONTEXT ( 'automotive_design' ) ;
#5559=DIRECTION ( 'NONE',  ( -0.9998870921963913805, -0.01502673813723916056, 0.000000000000000000 ) ) ;
#5775=DIRECTION ( 'NONE',  ( 1.000000000000000000, 0.000000000000000000, 0.000000000000000000 ) ) ;
#5783=AXIS2_PLACEMENT_3D ( 'NONE', #16040, #4532, #16294 ) ;
#5788=FACE_OUTER_BOUND ( 'NONE', #12475, .T. ) ;
#5797=CARTESIAN_POINT ( 'NONE',  ( 437.7731165870194445, 329.6061121441327941, -6.736600000000000144 ) ) ;
#5815=CARTESIAN_POINT ( 'NONE',  ( 437.7731165870194445, 329.6061121441327941, -6.736600000000000144 ) ) ;
#5861=EDGE_CURVE ( 'NONE', #4858, #16000, #13663, .T. ) ;
#5896=DIRECTION ( 'NONE',  ( 0.000000000000000000, 0.000000000000000000, 1.000000000000000000 ) ) ;
#5908=DIRECTION ( 'NONE',  ( 1.000000000000000000, 0.000000000000000000, 0.000000000000000000 ) ) ;
#5939=EDGE_CURVE ( 'NONE', #9126, #16083, #9086, .T. ) ;
#5942=VERTEX_POINT ( 'NONE', #14247 ) ;
#6067=LINE ( 'NONE', #6156, #7651 ) ;
#6082=AXIS2_PLACEMENT_3D ( 'NONE', #9152, #12763, #10278 ) ;
#6156=CARTESIAN_POINT ( 'NONE',  ( 39.09977993252485362, 344.7110430980827687, -6.736600000000000144 ) ) ;
#6215=DIRECTION ( 'NONE',  ( 1.000000000000000000, 0.000000000000000000, 0.000000000000000000 ) ) ;
#6246=CARTESIAN_POINT ( 'NONE',  ( 415.0210210471910841, 329.6061121441327941, 0.000000000000000000 ) ) ;
#6268=VERTEX_POINT ( 'NONE', #8656 ) ;
#6279=LINE ( 'NONE', #13005, #8602 ) ;
#6291=DIRECTION ( 'NONE',  ( 0.000000000000000000, 0.000000000000000000, 1.000000000000000000 ) ) ;
#6301=CARTESIAN_POINT ( 'NONE',  ( 415.0210210471910841, 329.6061121441327941, -6.736600000000000144 ) ) ;
#6335=CARTESIAN_POINT ( 'NONE',  ( 39.41161623800082481, 323.9612906317821057, -10.00000000000000000 ) ) ;
#6403=DIRECTION ( 'NONE',  ( 0.000000000000000000, 0.000000000000000000, 1.000000000000000000 ) ) ;
#6516=EDGE_CURVE ( 'NONE', #4443, #3814, #12238, .T. ) ;
#6711=CARTESIAN_POINT ( 'NONE',  ( 39.41161623800082481, 323.9612906317821057, 0.000000000000000000 ) ) ;
#6750=FACE_OUTER_BOUND ( 'NONE', #4204, .T. ) ;
#6751=DIRECTION ( 'NONE',  ( 0.000000000000000000, 0.000000000000000000, 1.000000000000000000 ) ) ;
#6769=ORIENTED_EDGE ( 'NONE', *, *, #5861, .T. ) ;
#6829=LINE ( 'NONE', #2809, #11065 ) ;
#6986=ORIENTED_EDGE ( 'NONE', *, *, #2516, .F. ) ;
#6990=CARTESIAN_POINT ( 'NONE',  ( 39.06972645625037899, 346.7108172824755457, -6.736600000000000144 ) ) ;
#7027=EDGE_LOOP ( 'NONE', ( #13477, #192, #14781, #11541 ) ) ;
#7077=LINE ( 'NONE', #5797, #13782 ) ;
#7107=ORIENTED_EDGE ( 'NONE', *, *, #4237, .T. ) ;
#7110=DIRECTION ( 'NONE',  ( 0.9998870921963913805, 0.01502673813723915709, 0.000000000000000000 ) ) ;
#7113=DIRECTION ( 'NONE',  ( 0.000000000000000000, 0.000000000000000000, 1.000000000000000000 ) ) ;
#7131=FACE_OUTER_BOUND ( 'NONE', #9143, .T. ) ;
#7148=ADVANCED_FACE ( 'NONE', ( #8932, #7621 ), #14251, .T. ) ;
#7276=VERTEX_POINT ( 'NONE', #5049 ) ;
#7312=LINE ( 'NONE', #8525, #4497 ) ;
#7350=PRODUCT_DEFINITION ( 'UNKNOWN', '', #8910, #4860 ) ;
#7408=VERTEX_POINT ( 'NONE', #5815 ) ;
#7412=CARTESIAN_POINT ( 'NONE',  ( 39.41161623800082481, 323.9612906317821057, -6.736600000000000144 ) ) ;
#7455=DIRECTION ( 'NONE',  ( 1.000000000000000000, 0.000000000000000000, 0.000000000000000000 ) ) ;
#7462=ORIENTED_EDGE ( 'NONE', *, *, #716, .T. ) ;
#7480=CIRCLE ( 'NONE', #4762, 20.75209553982837463 ) ;
#7505=AXIS2_PLACEMENT_3D ( 'NONE', #10061, #15299, #16579 ) ;
#7508=ORIENTED_EDGE ( 'NONE', *, *, #90, .F. ) ;
#7509=PRODUCT_DEFINITION_SHAPE ( 'NONE', 'NONE',  #7350 ) ;
#7553=ORIENTED_EDGE ( 'NONE', *, *, #4237, .F. ) ;
#7593=DIRECTION ( 'NONE',  ( 1.000000000000000000, 0.000000000000000000, 0.000000000000000000 ) ) ;
#7621=FACE_OUTER_BOUND ( 'NONE', #7922, .T. ) ;
#7651=VECTOR ( 'NONE', #2044, 1000.000000000000114 ) ;
#7676=SHAPE_REPRESENTATION ( 'Part9^Assem2', ( #1488 ), #14944 ) ;
#7726=LINE ( 'NONE', #5150, #14647 ) ;
#7841=VECTOR ( 'NONE', #6403, 1000.000000000000000 ) ;
#7902=EDGE_CURVE ( 'NONE', #9126, #4738, #11041, .T. ) ;
#7922=EDGE_LOOP ( 'NONE', ( #8142, #2048, #14367, #14424, #3046 ) ) ;
#7977=ORIENTED_EDGE ( 'NONE', *, *, #14943, .F. ) ;
#8079=FILL_AREA_STYLE_COLOUR ( '', #8344 ) ;
#8100=DIRECTION ( 'NONE',  ( 1.000000000000000000, 0.000000000000000000, 0.000000000000000000 ) ) ;
#8130=VERTEX_POINT ( 'NONE', #14547 ) ;
#8142=ORIENTED_EDGE ( 'NONE', *, *, #14119, .T. ) ;
#8161=ORIENTED_EDGE ( 'NONE', *, *, #5939, .T. ) ;
#8247=EDGE_CURVE ( 'NONE', #16000, #8130, #14476, .T. ) ;
#8263=LINE ( 'NONE', #1308, #15738 ) ;
#8290=CIRCLE ( 'NONE', #6082, 22.75209553982836397 ) ;
#8344=COLOUR_RGB ( '', 0.40784314, 0.44705882, 0.49803922) ;
#8368=ORIENTED_EDGE ( 'NONE', *, *, #5861, .F. ) ;
#8395=DIRECTION ( 'NONE',  ( 0.000000000000000000, 0.000000000000000000, 1.000000000000000000 ) ) ;
#8414=VERTEX_POINT ( 'NONE', #14175 ) ;
#8430=ORIENTED_EDGE ( 'NONE', *, *, #2898, .F. ) ;
#8459=DIRECTION ( 'NONE',  ( 0.9998870921963913805, 0.01502673813723916056, 0.000000000000000000 ) ) ;
#8473=FACE_BOUND ( 'NONE', #16772, .T. ) ;
#8509=AXIS2_PLACEMENT_3D ( 'NONE', #7412, #8395, #16526 ) ;
#8525=CARTESIAN_POINT ( 'NONE',  ( 415.3629108289414944, 306.8565854934392974, -6.736600000000000144 ) ) ;
#8602=VECTOR ( 'NONE', #5248, 1000.000000000000000 ) ;
#8626=MECHANICAL_DESIGN_GEOMETRIC_PRESENTATION_REPRESENTATION('',(#11632),#16833);
#8656=CARTESIAN_POINT ( 'NONE',  ( 415.3328573526671335, 308.8563596778320743, -6.736600000000000144 ) ) ;
#8693=DIRECTION ( 'NONE',  ( 0.000000000000000000, 0.000000000000000000, 1.000000000000000000 ) ) ;
#8708=ORIENTED_EDGE ( 'NONE', *, *, #12222, .F. ) ;
#8771=CARTESIAN_POINT ( 'NONE',  ( 415.0210210471910841, 329.6061121441327941, -10.00000000000000000 ) ) ;
#8814=ORIENTED_EDGE ( 'NONE', *, *, #14119, .F. ) ;
#8899=ORIENTED_EDGE ( 'NONE', *, *, #9882, .F. ) ;
#8910=PRODUCT_DEFINITION_FORMATION_WITH_SPECIFIED_SOURCE ( 'ANY', '', #3694, .NOT_KNOWN. ) ;
#8932=FACE_BOUND ( 'NONE', #1668, .T. ) ;
#8942=CARTESIAN_POINT ( 'NONE',  ( 415.3328573526671335, 308.8563596778320743, 0.000000000000000000 ) ) ;
#8991=ORIENTED_EDGE ( 'NONE', *, *, #12740, .F. ) ;
#9047=ADVANCED_FACE ( 'NONE', ( #8473, #10095 ), #15159, .F. ) ;
#9086=LINE ( 'NONE', #12950, #7841 ) ;
#9091=DIRECTION ( 'NONE',  ( 1.000000000000000000, 0.000000000000000000, -0.000000000000000000 ) ) ;
#9093=CIRCLE ( 'NONE', #14299, 22.75209553982837463 ) ;
#9123=( NAMED_UNIT ( * ) PLANE_ANGLE_UNIT ( ) SI_UNIT ( $, .RADIAN. ) );
#9126=VERTEX_POINT ( 'NONE', #11459 ) ;
#9143=EDGE_LOOP ( 'NONE', ( #7107, #7462, #5154, #16116 ) ) ;
#9148=DIRECTION ( 'NONE',  ( -0.9998870921963913805, -0.01502673813723916230, -0.000000000000000000 ) ) ;
#9152=CARTESIAN_POINT ( 'NONE',  ( 39.41161623800082481, 323.9612906317821057, 0.000000000000000000 ) ) ;
#9259=DIRECTION ( 'NONE',  ( 1.000000000000000000, 0.000000000000000000, 0.000000000000000000 ) ) ;
#9316=CARTESIAN_POINT ( 'NONE',  ( 39.06972645625037899, 346.7108172824755457, 0.000000000000000000 ) ) ;
#9323=PLANE ( 'NONE',  #9980 ) ;
#9371=( NAMED_UNIT ( * ) SI_UNIT ( $, .STERADIAN. ) SOLID_ANGLE_UNIT ( ) );
#9388=CARTESIAN_POINT ( 'NONE',  ( 39.41161623800082481, 323.9612906317821057, -6.736600000000000144 ) ) ;
#9493=LINE ( 'NONE', #9316, #1256 ) ;
#9551=EDGE_CURVE ( 'NONE', #2249, #5942, #11538, .T. ) ;
#9568=ADVANCED_FACE ( 'NONE', ( #6750 ), #3534, .F. ) ;
#9615=CARTESIAN_POINT ( 'NONE',  ( 415.0210210471910841, 329.6061121441327941, 0.000000000000000000 ) ) ;
#9623=EDGE_CURVE ( 'NONE', #6268, #1132, #14566, .T. ) ;
#9733=CIRCLE ( 'NONE', #7505, 22.75209553982837463 ) ;
#9739=EDGE_LOOP ( 'NONE', ( #2781, #14620, #11067, #10578 ) ) ;
#9846=EDGE_CURVE ( 'NONE', #1132, #8130, #11137, .T. ) ;
#9882=EDGE_CURVE ( 'NONE', #7408, #15471, #9093, .T. ) ;
#9939=AXIS2_PLACEMENT_3D ( 'NONE', #9615, #14851, #12193 ) ;
#9950=CARTESIAN_POINT ( 'NONE',  ( 415.0210210471910841, 329.6061121441327941, -10.00000000000000000 ) ) ;
#9980=AXIS2_PLACEMENT_3D ( 'NONE', #4165, #11200, #8459 ) ;
#9998=EDGE_LOOP ( 'NONE', ( #5447, #6769, #13361, #4403 ) ) ;
#10061=CARTESIAN_POINT ( 'NONE',  ( 415.0210210471910841, 329.6061121441327941, -6.736600000000000144 ) ) ;
#10084=CARTESIAN_POINT ( 'NONE',  ( 39.06972645625037899, 346.7108172824755457, 0.000000000000000000 ) ) ;
#10089=ADVANCED_FACE ( 'NONE', ( #5788 ), #14901, .T. ) ;
#10095=FACE_OUTER_BOUND ( 'NONE', #2059, .T. ) ;
#10179=VERTEX_POINT ( 'NONE', #10084 ) ;
#10193=VECTOR ( 'NONE', #2993, 1000.000000000000000 ) ;
#10278=DIRECTION ( 'NONE',  ( 1.000000000000000000, 0.000000000000000000, 0.000000000000000000 ) ) ;
#10315=DIRECTION ( 'NONE',  ( -0.000000000000000000, -0.000000000000000000, 1.000000000000000000 ) ) ;
#10355=AXIS2_PLACEMENT_3D ( 'NONE', #6246, #4417, #2140 ) ;
#10369=PLANE ( 'NONE',  #12409 ) ;
#10506=ORIENTED_EDGE ( 'NONE', *, *, #2887, .F. ) ;
#10511=ORIENTED_EDGE ( 'NONE', *, *, #9623, .F. ) ;
#10578=ORIENTED_EDGE ( 'NONE', *, *, #6516, .F. ) ;
#10792=CARTESIAN_POINT ( 'NONE',  ( 39.06972645625037899, 346.7108172824755457, -6.736600000000000144 ) ) ;
#10840=PRODUCT_CONTEXT ( 'NONE', #5555, 'mechanical' ) ;
#11002=AXIS2_PLACEMENT_3D ( 'NONE', #8771, #4022, #7455 ) ;
#11041=LINE ( 'NONE', #16282, #2107 ) ;
#11065=VECTOR ( 'NONE', #6751, 1000.000000000000000 ) ;
#11067=ORIENTED_EDGE ( 'NONE', *, *, #2385, .F. ) ;
#11069=VECTOR ( 'NONE', #12289, 1000.000000000000000 ) ;
#11104=DIRECTION ( 'NONE',  ( 0.000000000000000000, 0.000000000000000000, 1.000000000000000000 ) ) ;
#11137=LINE ( 'NONE', #14051, #3045 ) ;
#11200=DIRECTION ( 'NONE',  ( 0.01502673813723916056, -0.9998870921963913805, 0.000000000000000000 ) ) ;
#11229=FACE_OUTER_BOUND ( 'NONE', #12068, .T. ) ;
#11264=DIRECTION ( 'NONE',  ( 0.000000000000000000, 0.000000000000000000, 1.000000000000000000 ) ) ;
#11459=CARTESIAN_POINT ( 'NONE',  ( 39.75350601975127063, 301.2117639810886089, -6.736600000000000144 ) ) ;
#11538=CIRCLE ( 'NONE', #2486, 22.75209553982837463 ) ;
#11541=ORIENTED_EDGE ( 'NONE', *, *, #2816, .T. ) ;
#11632=STYLED_ITEM ( 'NONE', ( #359 ), #3067 ) ;
#11672=VERTEX_POINT ( 'NONE', #15648 ) ;
#11833=DIRECTION ( 'NONE',  ( -0.01502673813723916056, 0.9998870921963913805, 0.000000000000000000 ) ) ;
#11928=CARTESIAN_POINT ( 'NONE',  ( 414.7091847417151484, 350.3558646104334571, 0.000000000000000000 ) ) ;
#11936=ADVANCED_FACE ( 'NONE', ( #7131 ), #4820, .T. ) ;
#11963=AXIS2_PLACEMENT_3D ( 'NONE', #6711, #15785, #9091 ) ;
#12039=CIRCLE ( 'NONE', #15047, 22.75209553982836397 ) ;
#12068=EDGE_LOOP ( 'NONE', ( #3464, #10511, #1706, #4257 ) ) ;
#12099=CARTESIAN_POINT ( 'NONE',  ( 414.7091847417151484, 350.3558646104334571, -6.736600000000000144 ) ) ;
#12118=ORIENTED_EDGE ( 'NONE', *, *, #2516, .T. ) ;
#12120=SURFACE_STYLE_FILL_AREA ( #4396 ) ;
#12129=EDGE_CURVE ( 'NONE', #3814, #6268, #14442, .T. ) ;
#12193=DIRECTION ( 'NONE',  ( 1.000000000000000000, 0.000000000000000000, 0.000000000000000000 ) ) ;
#12222=EDGE_CURVE ( 'NONE', #3705, #10179, #444, .T. ) ;
#12238=CIRCLE ( 'NONE', #448, 20.75209553982835331 ) ;
#12289=DIRECTION ( 'NONE',  ( 0.000000000000000000, 0.000000000000000000, 1.000000000000000000 ) ) ;
#12409=AXIS2_PLACEMENT_3D ( 'NONE', #1011, #5274, #3673 ) ;
#12440=ORIENTED_EDGE ( 'NONE', *, *, #716, .F. ) ;
#12475=EDGE_LOOP ( 'NONE', ( #1385, #7977, #12118, #2944 ) ) ;
#12581=DIRECTION ( 'NONE',  ( 0.9998870921963913805, 0.01502673813723916230, 0.000000000000000000 ) ) ;
#12609=ORIENTED_EDGE ( 'NONE', *, *, #2887, .T. ) ;
#12618=ADVANCED_BREP_SHAPE_REPRESENTATION ( '', ( #3067, #1488 ), #14944 ) ;
#12624=ADVANCED_FACE ( 'NONE', ( #13394 ), #15865, .F. ) ;
#12740=EDGE_CURVE ( 'NONE', #11672, #7276, #14505, .T. ) ;
#12763=DIRECTION ( 'NONE',  ( 0.000000000000000000, 0.000000000000000000, 1.000000000000000000 ) ) ;
#12778=FACE_OUTER_BOUND ( 'NONE', #7027, .T. ) ;
#12949=ADVANCED_FACE ( 'NONE', ( #5186 ), #15597, .T. ) ;
#12950=CARTESIAN_POINT ( 'NONE',  ( 39.75350601975127063, 301.2117639810886089, -6.736600000000000144 ) ) ;
#12992=SHAPE_REPRESENTATION_RELATIONSHIP ( 'NONE' , 'NONE' ,  #7676, #12618 ) ;
#13005=CARTESIAN_POINT ( 'NONE',  ( 39.06972645625037899, 346.7108172824755457, -6.736600000000000144 ) ) ;
#13123=CARTESIAN_POINT ( 'NONE',  ( 415.0210210471910841, 329.6061121441327941, 0.000000000000000000 ) ) ;
#13161=ORIENTED_EDGE ( 'NONE', *, *, #90, .T. ) ;
#13361=ORIENTED_EDGE ( 'NONE', *, *, #1, .F. ) ;
#13394=FACE_OUTER_BOUND ( 'NONE', #14603, .T. ) ;
#13430=SHAPE_DEFINITION_REPRESENTATION ( #7509, #7676 ) ;
#13477=ORIENTED_EDGE ( 'NONE', *, *, #15763, .F. ) ;
#13585=CARTESIAN_POINT ( 'NONE',  ( 39.06972645625037899, 346.7108172824755457, -6.736600000000000144 ) ) ;
#13663=LINE ( 'NONE', #1887, #2366 ) ;
#13739=EDGE_CURVE ( 'NONE', #3294, #4443, #6067, .T. ) ;
#13782=VECTOR ( 'NONE', #15000, 1000.000000000000000 ) ;
#13784=CIRCLE ( 'NONE', #3637, 20.75209553982835331 ) ;
#13832=DIRECTION ( 'NONE',  ( 1.000000000000000000, 0.000000000000000000, 0.000000000000000000 ) ) ;
#14051=CARTESIAN_POINT ( 'NONE',  ( 435.7731165870194445, 329.6061121441327941, -10.00000000000000000 ) ) ;
#14119=EDGE_CURVE ( 'NONE', #10179, #16083, #8290, .T. ) ;
#14130=EDGE_CURVE ( 'NONE', #7276, #4858, #13784, .T. ) ;
#14142=DIRECTION ( 'NONE',  ( -0.000000000000000000, -0.000000000000000000, 1.000000000000000000 ) ) ;
#14175=CARTESIAN_POINT ( 'NONE',  ( 415.3629108289414944, 306.8565854934392974, 0.000000000000000000 ) ) ;
#14184=CARTESIAN_POINT ( 'NONE',  ( 39.75350601975127063, 301.2117639810886089, 0.000000000000000000 ) ) ;
#14247=CARTESIAN_POINT ( 'NONE',  ( 414.6791312654406738, 352.3556387948262341, 0.000000000000000000 ) ) ;
#14251=PLANE ( 'NONE',  #11963 ) ;
#14299=AXIS2_PLACEMENT_3D ( 'NONE', #4933, #5896, #4607 ) ;
#14367=ORIENTED_EDGE ( 'NONE', *, *, #1317, .T. ) ;
#14424=ORIENTED_EDGE ( 'NONE', *, *, #9551, .T. ) ;
#14442=LINE ( 'NONE', #99, #16007 ) ;
#14476=CIRCLE ( 'NONE', #10355, 20.75209553982837463 ) ;
#14505=LINE ( 'NONE', #11928, #16720 ) ;
#14539=AXIS2_PLACEMENT_3D ( 'NONE', #6301, #3584, #1009 ) ;
#14547=CARTESIAN_POINT ( 'NONE',  ( 435.7731165870194445, 329.6061121441327941, 0.000000000000000000 ) ) ;
#14566=CIRCLE ( 'NONE', #5783, 20.75209553982837463 ) ;
#14603=EDGE_LOOP ( 'NONE', ( #13161, #5466, #8430, #2438 ) ) ;
#14620=ORIENTED_EDGE ( 'NONE', *, *, #14130, .T. ) ;
#14647=VECTOR ( 'NONE', #15722, 1000.000000000000000 ) ;
#14655=ORIENTED_EDGE ( 'NONE', *, *, #12129, .T. ) ;
#14707=ORIENTED_EDGE ( 'NONE', *, *, #13739, .T. ) ;
#14750=CARTESIAN_POINT ( 'NONE',  ( 39.72345254347677468, 303.2115381654813859, -6.736600000000000144 ) ) ;
#14781=ORIENTED_EDGE ( 'NONE', *, *, #7902, .T. ) ;
#14830=AXIS2_PLACEMENT_3D ( 'NONE', #1617, #11833, #5559 ) ;
#14849=DIRECTION ( 'NONE',  ( 1.000000000000000000, 0.000000000000000000, 0.000000000000000000 ) ) ;
#14851=DIRECTION ( 'NONE',  ( 0.000000000000000000, 0.000000000000000000, 1.000000000000000000 ) ) ;
#14901=PLANE ( 'NONE',  #16489 ) ;
#14943=EDGE_CURVE ( 'NONE', #15471, #5942, #6829, .T. ) ;
#14944=( GEOMETRIC_REPRESENTATION_CONTEXT ( 3 ) GLOBAL_UNCERTAINTY_ASSIGNED_CONTEXT ( ( #15175 ) ) GLOBAL_UNIT_ASSIGNED_CONTEXT ( ( #1387, #9123, #113 ) ) REPRESENTATION_CONTEXT ( 'NONE', 'WORKASPACE' ) );
#14975=DIRECTION ( 'NONE',  ( 0.000000000000000000, 0.000000000000000000, 1.000000000000000000 ) ) ;
#14990=DIRECTION ( 'NONE',  ( -0.01502673813723916403, 0.9998870921963913805, 0.000000000000000000 ) ) ;
#15000=DIRECTION ( 'NONE',  ( 0.000000000000000000, 0.000000000000000000, 1.000000000000000000 ) ) ;
#15047=AXIS2_PLACEMENT_3D ( 'NONE', #15205, #7113, #13832 ) ;
#15159=PLANE ( 'NONE',  #8509 ) ;
#15175=UNCERTAINTY_MEASURE_WITH_UNIT (LENGTH_MEASURE( 1.000000000000000082E-05 ), #1387, 'distance_accuracy_value', 'NONE');
#15186=DIRECTION ( 'NONE',  ( -0.000000000000000000, -0.000000000000000000, 1.000000000000000000 ) ) ;
#15205=CARTESIAN_POINT ( 'NONE',  ( 39.41161623800082481, 323.9612906317821057, -6.736600000000000144 ) ) ;
#15217=DIRECTION ( 'NONE',  ( 1.000000000000000000, 0.000000000000000000, 0.000000000000000000 ) ) ;
#15229=DIRECTION ( 'NONE',  ( 0.000000000000000000, 0.000000000000000000, 1.000000000000000000 ) ) ;
#15248=ADVANCED_FACE ( 'NONE', ( #3665 ), #2361, .T. ) ;
#15299=DIRECTION ( 'NONE',  ( 0.000000000000000000, 0.000000000000000000, 1.000000000000000000 ) ) ;
#15397=ORIENTED_EDGE ( 'NONE', *, *, #1958, .F. ) ;
#15421=CIRCLE ( 'NONE', #1236, 20.75209553982837463 ) ;
#15438=ADVANCED_FACE ( 'NONE', ( #4086 ), #9323, .F. ) ;
#15471=VERTEX_POINT ( 'NONE', #1850 ) ;
#15472=DIRECTION ( 'NONE',  ( 0.9998870921963913805, 0.01502673813723916056, -0.000000000000000000 ) ) ;
#15516=CARTESIAN_POINT ( 'NONE',  ( 39.41161623800082481, 323.9612906317821057, -6.736600000000000144 ) ) ;
#15555=DIRECTION ( 'NONE',  ( 1.000000000000000000, 0.000000000000000000, 0.000000000000000000 ) ) ;
#15597=CYLINDRICAL_SURFACE ( 'NONE', #14539, 22.75209553982837463 ) ;
#15648=CARTESIAN_POINT ( 'NONE',  ( 414.7091847417151484, 350.3558646104334571, 0.000000000000000000 ) ) ;
#15722=DIRECTION ( 'NONE',  ( -0.000000000000000000, -0.000000000000000000, 1.000000000000000000 ) ) ;
#15738=VECTOR ( 'NONE', #1486, 1000.000000000000000 ) ;
#15763=EDGE_CURVE ( 'NONE', #16083, #8414, #8263, .T. ) ;
#15785=DIRECTION ( 'NONE',  ( 0.000000000000000000, 0.000000000000000000, 1.000000000000000000 ) ) ;
#15865=PLANE ( 'NONE',  #14830 ) ;
#15978=( LENGTH_UNIT ( ) NAMED_UNIT ( * ) SI_UNIT ( .MILLI., .METRE. ) );
#16000=VERTEX_POINT ( 'NONE', #8942 ) ;
#16007=VECTOR ( 'NONE', #15472, 1000.000000000000114 ) ;
#16040=CARTESIAN_POINT ( 'NONE',  ( 415.0210210471910841, 329.6061121441327941, -6.736600000000000144 ) ) ;
#16083=VERTEX_POINT ( 'NONE', #14184 ) ;
#16116=ORIENTED_EDGE ( 'NONE', *, *, #2816, .F. ) ;
#16140=ADVANCED_FACE ( 'NONE', ( #2403 ), #1120, .F. ) ;
#16216=DIRECTION ( 'NONE',  ( 0.000000000000000000, 0.000000000000000000, 1.000000000000000000 ) ) ;
#16219=CARTESIAN_POINT ( 'NONE',  ( 415.3629108289414944, 306.8565854934392974, -6.736600000000000144 ) ) ;
#16258=CARTESIAN_POINT ( 'NONE',  ( 415.0210210471910841, 329.6061121441327941, -6.736600000000000144 ) ) ;
#16282=CARTESIAN_POINT ( 'NONE',  ( 39.75350601975127063, 301.2117639810886089, -6.736600000000000144 ) ) ;
#16294=DIRECTION ( 'NONE',  ( 1.000000000000000000, 0.000000000000000000, 0.000000000000000000 ) ) ;
#16464=CYLINDRICAL_SURFACE ( 'NONE', #426, 20.75209553982837463 ) ;
#16489=AXIS2_PLACEMENT_3D ( 'NONE', #6990, #14990, #396 ) ;
#16526=DIRECTION ( 'NONE',  ( 1.000000000000000000, 0.000000000000000000, -0.000000000000000000 ) ) ;
#16579=DIRECTION ( 'NONE',  ( 1.000000000000000000, 0.000000000000000000, 0.000000000000000000 ) ) ;
#16720=VECTOR ( 'NONE', #2727, 1000.000000000000000 ) ;
#16772=EDGE_LOOP ( 'NONE', ( #14655, #2355, #12609, #14707, #2324 ) ) ;
#16833=( GEOMETRIC_REPRESENTATION_CONTEXT ( 3 ) GLOBAL_UNCERTAINTY_ASSIGNED_CONTEXT ( ( #2112 ) ) GLOBAL_UNIT_ASSIGNED_CONTEXT ( ( #15978, #450, #9371 ) ) REPRESENTATION_CONTEXT ( 'NONE', 'WORKASPACE' ) );
#16892=ORIENTED_EDGE ( 'NONE', *, *, #1958, .T. ) ;
ENDSEC;
END-ISO-10303-21;
